ISO-10303-21;
HEADER;
/* Generated by software containing ST-Developer
 * from STEP Tools, Inc. (www.steptools.com) 
 */

FILE_DESCRIPTION(
/* description */ ('CAx-IF Rec.Pracs.---Representation and Presentation of Product Manufa
cturing Information (PMI)---4.0---2014-10-13'),
/* implementation_level */ '2;1');

FILE_NAME(
/* name */ 'Socket Screw 3.step',
/* time_stamp */ '2026-10-24T18:52:33-07:00',
/* author */ (''),
/* organization */ (''),
/* preprocessor_version */ 'ST-DEVELOPER v20.2',
/* originating_system */ 'Autodesk Translation Framework v15.17.0.0',
/* authorisation */ '');

FILE_SCHEMA (('AP242_MANAGED_MODEL_BASED_3D_ENGINEERING_MIM_LF { 1 0 10303 442 2 1 4 }'));
ENDSEC;

DATA;
#10=MECHANICAL_DESIGN_GEOMETRIC_PRESENTATION_REPRESENTATION('',(#430),#34876);
#364=SHAPE_REPRESENTATION_RELATIONSHIP('SRR','None',#35001,#397);
#397=ADVANCED_BREP_SHAPE_REPRESENTATION('',(#463),#34859);
#430=STYLED_ITEM('',(#35164),#463);
#463=MANIFOLD_SOLID_BREP('Socket Screw 3',#19570);
#893=PLANE('',#21261);
#894=PLANE('',#21262);
#895=PLANE('',#21266);
#896=PLANE('',#21267);
#897=PLANE('',#21268);
#898=PLANE('',#21269);
#899=PLANE('',#21270);
#900=PLANE('',#21271);
#1985=LINE('',#32072,#3584);
#1986=LINE('',#32074,#3585);
#1987=LINE('',#32076,#3586);
#1988=LINE('',#32077,#3587);
#1989=LINE('',#32080,#3588);
#1990=LINE('',#32082,#3589);
#1991=LINE('',#32083,#3590);
#1992=LINE('',#32087,#3591);
#1993=LINE('',#32091,#3592);
#1994=LINE('',#32094,#3593);
#1995=LINE('',#32095,#3594);
#1996=LINE('',#32098,#3595);
#1997=LINE('',#32100,#3596);
#1998=LINE('',#32101,#3597);
#1999=LINE('',#32104,#3598);
#2000=LINE('',#32105,#3599);
#2001=LINE('',#32108,#3600);
#2002=LINE('',#32109,#3601);
#2003=LINE('',#32111,#3602);
#3584=VECTOR('',#25782,1.);
#3585=VECTOR('',#25783,1.);
#3586=VECTOR('',#25784,1.);
#3587=VECTOR('',#25785,1.);
#3588=VECTOR('',#25788,1.);
#3589=VECTOR('',#25789,1.);
#3590=VECTOR('',#25790,1.);
#3591=VECTOR('',#25793,1.);
#3592=VECTOR('',#25796,1.);
#3593=VECTOR('',#25801,1.);
#3594=VECTOR('',#25802,1.);
#3595=VECTOR('',#25805,1.);
#3596=VECTOR('',#25806,1.);
#3597=VECTOR('',#25807,1.);
#3598=VECTOR('',#25810,1.);
#3599=VECTOR('',#25811,1.);
#3600=VECTOR('',#25814,1.);
#3601=VECTOR('',#25815,1.);
#3602=VECTOR('',#25818,1.);
#4562=CYLINDRICAL_SURFACE('',#21263,0.0005);
#5395=FACE_OUTER_BOUND('',#6516,.T.);
#5396=FACE_OUTER_BOUND('',#6517,.T.);
#5397=FACE_OUTER_BOUND('',#6518,.T.);
#5398=FACE_OUTER_BOUND('',#6519,.T.);
#5399=FACE_OUTER_BOUND('',#6520,.T.);
#5400=FACE_OUTER_BOUND('',#6521,.T.);
#5401=FACE_OUTER_BOUND('',#6522,.T.);
#5402=FACE_OUTER_BOUND('',#6523,.T.);
#5403=FACE_OUTER_BOUND('',#6524,.T.);
#6516=EDGE_LOOP('',(#16034,#16035,#16036,#16037));
#6517=EDGE_LOOP('',(#16038,#16039,#16040,#16041));
#6518=EDGE_LOOP('',(#16042,#16043,#16044,#16045));
#6519=EDGE_LOOP('',(#16046,#16047,#16048,#16049));
#6520=EDGE_LOOP('',(#16050,#16051,#16052,#16053));
#6521=EDGE_LOOP('',(#16054,#16055,#16056,#16057,#16058,#16059,#16060));
#6522=EDGE_LOOP('',(#16061,#16062,#16063,#16064));
#6523=EDGE_LOOP('',(#16065,#16066,#16067,#16068,#16069,#16070,#16071));
#6524=EDGE_LOOP('',(#16072,#16073,#16074,#16075));
#7571=CIRCLE('',#21264,0.00050000000001);
#7572=CIRCLE('',#21265,0.00050000000001);
#9141=VERTEX_POINT('',#32070);
#9142=VERTEX_POINT('',#32071);
#9143=VERTEX_POINT('',#32073);
#9144=VERTEX_POINT('',#32075);
#9145=VERTEX_POINT('',#32079);
#9146=VERTEX_POINT('',#32081);
#9147=VERTEX_POINT('',#32085);
#9148=VERTEX_POINT('',#32086);
#9149=VERTEX_POINT('',#32088);
#9150=VERTEX_POINT('',#32090);
#9151=VERTEX_POINT('',#32097);
#9152=VERTEX_POINT('',#32099);
#9153=VERTEX_POINT('',#32103);
#9154=VERTEX_POINT('',#32107);
#11575=EDGE_CURVE('',#9141,#9142,#1985,.T.);
#11576=EDGE_CURVE('',#9142,#9143,#1986,.T.);
#11577=EDGE_CURVE('',#9143,#9144,#1987,.T.);
#11578=EDGE_CURVE('',#9141,#9144,#1988,.T.);
#11579=EDGE_CURVE('',#9145,#9143,#1989,.T.);
#11580=EDGE_CURVE('',#9146,#9145,#1990,.T.);
#11581=EDGE_CURVE('',#9144,#9146,#1991,.T.);
#11582=EDGE_CURVE('',#9147,#9148,#1992,.T.);
#11583=EDGE_CURVE('',#9147,#9149,#7571,.T.);
#11584=EDGE_CURVE('',#9149,#9150,#1993,.T.);
#11585=EDGE_CURVE('',#9148,#9150,#7572,.T.);
#11586=EDGE_CURVE('',#9149,#9146,#1994,.T.);
#11587=EDGE_CURVE('',#9150,#9145,#1995,.T.);
#11588=EDGE_CURVE('',#9151,#9148,#1996,.T.);
#11589=EDGE_CURVE('',#9152,#9151,#1997,.T.);
#11590=EDGE_CURVE('',#9147,#9152,#1998,.T.);
#11591=EDGE_CURVE('',#9153,#9152,#1999,.T.);
#11592=EDGE_CURVE('',#9141,#9153,#2000,.T.);
#11593=EDGE_CURVE('',#9154,#9153,#2001,.T.);
#11594=EDGE_CURVE('',#9142,#9154,#2002,.T.);
#11595=EDGE_CURVE('',#9151,#9154,#2003,.T.);
#16034=ORIENTED_EDGE('',*,*,#11575,.T.);
#16035=ORIENTED_EDGE('',*,*,#11576,.T.);
#16036=ORIENTED_EDGE('',*,*,#11577,.T.);
#16037=ORIENTED_EDGE('',*,*,#11578,.F.);
#16038=ORIENTED_EDGE('',*,*,#11577,.F.);
#16039=ORIENTED_EDGE('',*,*,#11579,.F.);
#16040=ORIENTED_EDGE('',*,*,#11580,.F.);
#16041=ORIENTED_EDGE('',*,*,#11581,.F.);
#16042=ORIENTED_EDGE('',*,*,#11582,.F.);
#16043=ORIENTED_EDGE('',*,*,#11583,.T.);
#16044=ORIENTED_EDGE('',*,*,#11584,.T.);
#16045=ORIENTED_EDGE('',*,*,#11585,.F.);
#16046=ORIENTED_EDGE('',*,*,#11584,.F.);
#16047=ORIENTED_EDGE('',*,*,#11586,.T.);
#16048=ORIENTED_EDGE('',*,*,#11580,.T.);
#16049=ORIENTED_EDGE('',*,*,#11587,.F.);
#16050=ORIENTED_EDGE('',*,*,#11588,.F.);
#16051=ORIENTED_EDGE('',*,*,#11589,.F.);
#16052=ORIENTED_EDGE('',*,*,#11590,.F.);
#16053=ORIENTED_EDGE('',*,*,#11582,.T.);
#16054=ORIENTED_EDGE('',*,*,#11590,.T.);
#16055=ORIENTED_EDGE('',*,*,#11591,.F.);
#16056=ORIENTED_EDGE('',*,*,#11592,.F.);
#16057=ORIENTED_EDGE('',*,*,#11578,.T.);
#16058=ORIENTED_EDGE('',*,*,#11581,.T.);
#16059=ORIENTED_EDGE('',*,*,#11586,.F.);
#16060=ORIENTED_EDGE('',*,*,#11583,.F.);
#16061=ORIENTED_EDGE('',*,*,#11592,.T.);
#16062=ORIENTED_EDGE('',*,*,#11593,.F.);
#16063=ORIENTED_EDGE('',*,*,#11594,.F.);
#16064=ORIENTED_EDGE('',*,*,#11575,.F.);
#16065=ORIENTED_EDGE('',*,*,#11594,.T.);
#16066=ORIENTED_EDGE('',*,*,#11595,.F.);
#16067=ORIENTED_EDGE('',*,*,#11588,.T.);
#16068=ORIENTED_EDGE('',*,*,#11585,.T.);
#16069=ORIENTED_EDGE('',*,*,#11587,.T.);
#16070=ORIENTED_EDGE('',*,*,#11579,.T.);
#16071=ORIENTED_EDGE('',*,*,#11576,.F.);
#16072=ORIENTED_EDGE('',*,*,#11595,.T.);
#16073=ORIENTED_EDGE('',*,*,#11593,.T.);
#16074=ORIENTED_EDGE('',*,*,#11591,.T.);
#16075=ORIENTED_EDGE('',*,*,#11589,.T.);
#19111=ADVANCED_FACE('',(#5395),#893,.T.);
#19112=ADVANCED_FACE('',(#5396),#894,.F.);
#19113=ADVANCED_FACE('',(#5397),#4562,.T.);
#19114=ADVANCED_FACE('',(#5398),#895,.F.);
#19115=ADVANCED_FACE('',(#5399),#896,.T.);
#19116=ADVANCED_FACE('',(#5400),#897,.T.);
#19117=ADVANCED_FACE('',(#5401),#898,.T.);
#19118=ADVANCED_FACE('',(#5402),#899,.T.);
#19119=ADVANCED_FACE('',(#5403),#900,.T.);
#19570=CLOSED_SHELL('',(#19111,#19112,#19113,#19114,#19115,#19116,#19117,
#19118,#19119));
#21260=AXIS2_PLACEMENT_3D('',#32068,#25778,#25779);
#21261=AXIS2_PLACEMENT_3D('',#32069,#25780,#25781);
#21262=AXIS2_PLACEMENT_3D('',#32078,#25786,#25787);
#21263=AXIS2_PLACEMENT_3D('',#32084,#25791,#25792);
#21264=AXIS2_PLACEMENT_3D('',#32089,#25794,#25795);
#21265=AXIS2_PLACEMENT_3D('',#32092,#25797,#25798);
#21266=AXIS2_PLACEMENT_3D('',#32093,#25799,#25800);
#21267=AXIS2_PLACEMENT_3D('',#32096,#25803,#25804);
#21268=AXIS2_PLACEMENT_3D('',#32102,#25808,#25809);
#21269=AXIS2_PLACEMENT_3D('',#32106,#25812,#25813);
#21270=AXIS2_PLACEMENT_3D('',#32110,#25816,#25817);
#21271=AXIS2_PLACEMENT_3D('',#32112,#25819,#25820);
#25778=DIRECTION('axis',(0.,0.,1.));
#25779=DIRECTION('refdir',(1.,0.,0.));
#25780=DIRECTION('center_axis',(1.,5.1420277733694E-16,-1.0522467400333E-14));
#25781=DIRECTION('ref_axis',(-1.0522467400333E-14,1.06077175752244E-14,
-1.));
#25782=DIRECTION('',(-1.00001914094642E-12,1.00113222673461E-12,1.));
#25783=DIRECTION('',(-9.47915311079142E-15,-1.,1.E-14));
#25784=DIRECTION('',(1.00001914094642E-12,-9.99999999998997E-13,-1.));
#25785=DIRECTION('',(-9.47915311079142E-15,-1.,1.E-14));
#25786=DIRECTION('center_axis',(-4.5961454925099E-16,1.,6.61092274672771E-17));
#25787=DIRECTION('ref_axis',(-1.05885766278003E-14,6.61092274672722E-17,
-1.));
#25788=DIRECTION('',(1.,-9.54038545074888E-15,9.9999999999998E-15));
#25789=DIRECTION('',(-9.56631913100564E-15,9.99999999999985E-15,1.));
#25790=DIRECTION('',(-1.,9.54038545074888E-15,-9.9999999999998E-15));
#25791=DIRECTION('center_axis',(0.,-4.29362650667545E-31,1.));
#25792=DIRECTION('ref_axis',(4.28756753891971E-16,-1.,-4.29362650667545E-31));
#25793=DIRECTION('',(-9.99999999999976E-15,-1.04336808689941E-14,1.));
#25794=DIRECTION('center_axis',(-1.99999999991998E-11,2.E-11,1.));
#25795=DIRECTION('ref_axis',(-1.99995712428458E-11,-1.,1.99999999996E-11));
#25796=DIRECTION('',(-9.56631913100564E-15,9.99999999999985E-15,1.));
#25797=DIRECTION('center_axis',(-1.99999999991998E-11,2.E-11,1.));
#25798=DIRECTION('ref_axis',(-1.99995712428458E-11,-1.,1.99999999996E-11));
#25799=DIRECTION('center_axis',(1.,5.2084688920845E-16,-1.0522467400333E-14));
#25800=DIRECTION('ref_axis',(-1.0522467400333E-14,1.01548957588061E-14,
-1.));
#25801=DIRECTION('',(-9.47915311079142E-15,-1.,1.E-14));
#25802=DIRECTION('',(-9.47915311079142E-15,-1.,1.E-14));
#25803=DIRECTION('center_axis',(-5.3389151001177E-16,1.,6.61092274672778E-17));
#25804=DIRECTION('ref_axis',(-1.06105803387953E-14,6.61092274672721E-17,
-1.));
#25805=DIRECTION('',(-1.,9.99485333130104E-13,-1.00005108521413E-12));
#25806=DIRECTION('',(-9.99999999998993E-13,1.00002200370999E-12,1.));
#25807=DIRECTION('',(1.,-9.99466108488984E-13,9.99906900405741E-13));
#25808=DIRECTION('center_axis',(-1.0522467400333E-14,2.19844233825538E-15,
-1.));
#25809=DIRECTION('ref_axis',(1.,-6.53116410123922E-15,-1.0522467400333E-14));
#25810=DIRECTION('',(9.99479153109799E-13,1.,1.00219844233724E-12));
#25811=DIRECTION('',(1.,-9.99466108488984E-13,9.99906900405741E-13));
#25812=DIRECTION('center_axis',(5.33891510011771E-16,-1.,2.20037109950003E-17));
#25813=DIRECTION('ref_axis',(-1.,-5.33891510011771E-16,1.0522467400333E-14));
#25814=DIRECTION('',(9.99999999998993E-13,-1.00002200370999E-12,-1.));
#25815=DIRECTION('',(1.,-9.99466108488984E-13,9.99906900405741E-13));
#25816=DIRECTION('center_axis',(9.30995932482184E-17,-4.41888838750562E-15,
1.));
#25817=DIRECTION('ref_axis',(1.,3.89820370584558E-15,-9.30995932482012E-17));
#25818=DIRECTION('',(-9.99479153109799E-13,-1.,-1.00441888838649E-12));
#25819=DIRECTION('center_axis',(1.,5.3389151001188E-16,-1.0522467400333E-14));
#25820=DIRECTION('ref_axis',(-1.0522467400333E-14,1.04954770345521E-14,
-1.));
#32068=CARTESIAN_POINT('',(0.,0.,0.));
#32069=CARTESIAN_POINT('Origin',(0.02115,-0.0223,-0.01175));
#32070=CARTESIAN_POINT('',(0.02115,-0.02545,-0.00325000000000007));
#32071=CARTESIAN_POINT('',(0.02115,-0.02545,-0.00275000000000007));
#32072=CARTESIAN_POINT('',(0.0211500000000101,-0.02545000000001,-0.00749999999999003));
#32073=CARTESIAN_POINT('',(0.02115,-0.0317,-0.00275000000000007));
#32074=CARTESIAN_POINT('',(0.0211500000000101,-0.02545000000001,-0.00274999999999008));
#32075=CARTESIAN_POINT('',(0.02115,-0.0317,-0.00325000000000007));
#32076=CARTESIAN_POINT('',(0.0211500000000101,-0.0317000000000099,-0.00549999999999003));
#32077=CARTESIAN_POINT('',(0.02115000000001,-0.02545000000001,-0.00324999999999007));
#32078=CARTESIAN_POINT('Origin',(0.02115,-0.0317,0.000749999999999928));
#32079=CARTESIAN_POINT('',(0.02065,-0.0317,-0.00275000000000007));
#32080=CARTESIAN_POINT('',(0.0206500000000101,-0.03170000000001,-0.00274999999999007));
#32081=CARTESIAN_POINT('',(0.02065,-0.0317,-0.00325000000000006));
#32082=CARTESIAN_POINT('',(0.0206500000000101,-0.03170000000001,-0.00274999999999007));
#32083=CARTESIAN_POINT('',(0.0206500000000101,-0.03170000000001,-0.00324999999999008));
#32084=CARTESIAN_POINT('Origin',(0.02115,-0.02545,-0.00300000000000007));
#32085=CARTESIAN_POINT('',(0.02115,-0.02495,-0.00325000000000007));
#32086=CARTESIAN_POINT('',(0.02115,-0.02495,-0.00275000000000007));
#32087=CARTESIAN_POINT('',(0.0211500000000101,-0.02495000000001,-0.00274999999999008));
#32088=CARTESIAN_POINT('',(0.02065,-0.02545,-0.00325000000000006));
#32089=CARTESIAN_POINT('Origin',(0.02115000000001,-0.02545000000001,-0.00324999999999007));
#32090=CARTESIAN_POINT('',(0.02065,-0.02545,-0.00275000000000007));
#32091=CARTESIAN_POINT('',(0.0206500000000101,-0.02545000000001,-0.00274999999999008));
#32092=CARTESIAN_POINT('Origin',(0.0211500000000101,-0.02545000000001,-0.00274999999999008));
#32093=CARTESIAN_POINT('Origin',(0.02065,-0.02545,-0.00275000000000007));
#32094=CARTESIAN_POINT('',(0.0206500000000101,-0.02545000000001,-0.00324999999999008));
#32095=CARTESIAN_POINT('',(0.0206500000000101,-0.02545000000001,-0.00274999999999008));
#32096=CARTESIAN_POINT('Origin',(0.0229,-0.02495,-0.00325000000000009));
#32097=CARTESIAN_POINT('',(0.0262,-0.02495,-0.00275000000000013));
#32098=CARTESIAN_POINT('',(0.0229000000000101,-0.02495000000001,-0.00274999999999008));
#32099=CARTESIAN_POINT('',(0.0262,-0.02495,-0.00325000000000012));
#32100=CARTESIAN_POINT('',(0.0262000000000101,-0.02495000000001,-0.00274999999999007));
#32101=CARTESIAN_POINT('',(0.0229000000000101,-0.02495000000001,-0.00324999999999007));
#32102=CARTESIAN_POINT('Origin',(0.0229,-0.02545,-0.00325000000000009));
#32103=CARTESIAN_POINT('',(0.0262,-0.02545,-0.00325000000000012));
#32104=CARTESIAN_POINT('',(0.0262000000000101,-0.02495000000001,-0.00324999999999008));
#32105=CARTESIAN_POINT('',(0.0229000000000101,-0.02545000000001,-0.00324999999999007));
#32106=CARTESIAN_POINT('Origin',(0.0229,-0.02545,-0.00275000000000009));
#32107=CARTESIAN_POINT('',(0.0262,-0.02545,-0.00275000000000013));
#32108=CARTESIAN_POINT('',(0.0262000000000101,-0.02545000000001,-0.00324999999999008));
#32109=CARTESIAN_POINT('',(0.0229000000000101,-0.02545000000001,-0.00274999999999008));
#32110=CARTESIAN_POINT('Origin',(0.0229,-0.02495,-0.00275000000000009));
#32111=CARTESIAN_POINT('',(0.0262000000000101,-0.02545000000001,-0.00274999999999008));
#32112=CARTESIAN_POINT('Origin',(0.0262,-0.0252,-0.00300000000000012));
#34824=UNCERTAINTY_MEASURE_WITH_UNIT(LENGTH_MEASURE(1.E-5),#34877,
'DISTANCE_ACCURACY_VALUE',
'Maximum model space distance between geometric entities at asserted c
onnectivities');
#34841=UNCERTAINTY_MEASURE_WITH_UNIT(LENGTH_MEASURE(1.E-5),#34877,
'DISTANCE_ACCURACY_VALUE',
'Maximum model space distance between geometric entities at asserted c
onnectivities');
#34859=(
GEOMETRIC_REPRESENTATION_CONTEXT(3)
GLOBAL_UNCERTAINTY_ASSIGNED_CONTEXT((#34824))
GLOBAL_UNIT_ASSIGNED_CONTEXT((#34877,#34878,#34879))
REPRESENTATION_CONTEXT('','3D')
);
#34876=(
GEOMETRIC_REPRESENTATION_CONTEXT(3)
GLOBAL_UNCERTAINTY_ASSIGNED_CONTEXT((#34841))
GLOBAL_UNIT_ASSIGNED_CONTEXT((#34877,#34878,#34879))
REPRESENTATION_CONTEXT('','3D')
);
#34877=(
LENGTH_UNIT()
NAMED_UNIT(*)
SI_UNIT($,.METRE.)
);
#34878=(
NAMED_UNIT(*)
PLANE_ANGLE_UNIT()
SI_UNIT($,.RADIAN.)
);
#34879=(
NAMED_UNIT(*)
SI_UNIT($,.STERADIAN.)
SOLID_ANGLE_UNIT()
);
#34897=SHAPE_DEFINITION_REPRESENTATION(#34931,#35001);
#34931=PRODUCT_DEFINITION_SHAPE('',$,#35036);
#35001=SHAPE_REPRESENTATION('',(#21260),#34859);
#35018=PRODUCT_DEFINITION_CONTEXT('part definition',#35122,'design');
#35036=PRODUCT_DEFINITION('Socket Screw 3','Socket Screw 3',#35070,#35018);
#35070=PRODUCT_DEFINITION_FORMATION('',$,#35141);
#35122=APPLICATION_CONTEXT('Managed model based 3d engineering');
#35123=PRODUCT_CONTEXT('part definition',#35122,'mechanical');
#35141=PRODUCT('Socket Screw 3','Socket Screw 3',
'LEGAL AND USAGE DISCLAIMER: this Data/Model is provided \X2\201C\X0\A
S IS\X2\201D\X0\ for informational and representational only. It is a 
geometric approximation and is NOT engineered, certified, or guarantee
d for dimensional accuracy, exact tolerances, or production-level prec
ision. Vendor disclaims all implied warranties including fitness for a
 particular purpose. DO NOT USE FOR DIRECT PHYSICAL MANUFACTURING, AUT
OMATED PRODUCTION, OR SAFETY-CRITICAL SYSTEMS without independent engi
neering verification and resolution of any design discrepancies.',(#35123));
#35164=PRESENTATION_STYLE_ASSIGNMENT((#35173));
#35173=SURFACE_STYLE_USAGE(.BOTH.,#35182);
#35182=SURFACE_SIDE_STYLE('',(#35191));
#35191=SURFACE_STYLE_FILL_AREA(#35200);
#35200=FILL_AREA_STYLE('Plastic - Matte (White)',(#35209));
#35209=FILL_AREA_STYLE_COLOUR('Plastic - Matte (White)',#35218);
#35218=COLOUR_RGB('Plastic - Matte (White)',0.964705882352941,0.964705882352941,
0.952941176470588);
ENDSEC;
END-ISO-10303-21;
